ISO-10303-21;
HEADER;
/* Generated by software containing ST-Developer
 * from STEP Tools, Inc. (www.steptools.com) 
 */

FILE_DESCRIPTION(
/* description */ ('STEP AP214'),
/* implementation_level */ '2;1');

FILE_NAME(
/* name */ 'Coupling Set Screw 2.step',
/* time_stamp */ '2026-11-15T14:55:55-08:00',
/* author */ (''),
/* organization */ (''),
/* preprocessor_version */ 'ST-DEVELOPER v20.2',
/* originating_system */ 'Autodesk Translation Framework v15.17.0.0',
/* authorisation */ '');

FILE_SCHEMA (('AUTOMOTIVE_DESIGN { 1 0 10303 214 3 1 1 }'));
ENDSEC;

DATA;
#10=MECHANICAL_DESIGN_GEOMETRIC_PRESENTATION_REPRESENTATION('',(#942),#57079);
#882=SHAPE_REPRESENTATION_RELATIONSHIP('SRR','None',#57270,#911);
#911=ADVANCED_BREP_SHAPE_REPRESENTATION('',(#979),#57062);
#942=STYLED_ITEM('',(#57444),#979);
#979=MANIFOLD_SOLID_BREP('Body1',#24542);
#1148=FACE_BOUND('',#4227,.T.);
#1600=PLANE('',#25808);
#1601=PLANE('',#25810);
#1602=PLANE('',#25813);
#1603=PLANE('',#25814);
#1604=PLANE('',#25815);
#1605=PLANE('',#25816);
#1606=PLANE('',#25817);
#1607=PLANE('',#25818);
#1608=PLANE('',#25819);
#2703=FACE_OUTER_BOUND('',#4226,.T.);
#2704=FACE_OUTER_BOUND('',#4228,.T.);
#2705=FACE_OUTER_BOUND('',#4229,.T.);
#2706=FACE_OUTER_BOUND('',#4230,.T.);
#2707=FACE_OUTER_BOUND('',#4231,.T.);
#2708=FACE_OUTER_BOUND('',#4232,.T.);
#2709=FACE_OUTER_BOUND('',#4233,.T.);
#2710=FACE_OUTER_BOUND('',#4234,.T.);
#2711=FACE_OUTER_BOUND('',#4235,.T.);
#2712=FACE_OUTER_BOUND('',#4236,.T.);
#4226=EDGE_LOOP('',(#18426));
#4227=EDGE_LOOP('',(#18427,#18428,#18429,#18430,#18431,#18432));
#4228=EDGE_LOOP('',(#18433));
#4229=EDGE_LOOP('',(#18434,#18435,#18436,#18437));
#4230=EDGE_LOOP('',(#18438,#18439,#18440,#18441,#18442,#18443));
#4231=EDGE_LOOP('',(#18444,#18445,#18446,#18447));
#4232=EDGE_LOOP('',(#18448,#18449,#18450,#18451));
#4233=EDGE_LOOP('',(#18452,#18453,#18454,#18455));
#4234=EDGE_LOOP('',(#18456,#18457,#18458,#18459));
#4235=EDGE_LOOP('',(#18460,#18461,#18462,#18463));
#4236=EDGE_LOOP('',(#18464,#18465,#18466,#18467));
#5845=LINE('',#52200,#7812);
#5846=LINE('',#52202,#7813);
#5847=LINE('',#52204,#7814);
#5848=LINE('',#52206,#7815);
#5849=LINE('',#52208,#7816);
#5850=LINE('',#52209,#7817);
#5851=LINE('',#52214,#7818);
#5852=LINE('',#52218,#7819);
#5853=LINE('',#52220,#7820);
#5854=LINE('',#52222,#7821);
#5855=LINE('',#52224,#7822);
#5856=LINE('',#52226,#7823);
#5857=LINE('',#52227,#7824);
#5858=LINE('',#52229,#7825);
#5859=LINE('',#52230,#7826);
#5860=LINE('',#52232,#7827);
#5861=LINE('',#52234,#7828);
#5862=LINE('',#52236,#7829);
#5863=LINE('',#52238,#7830);
#7812=VECTOR('',#29925,1000.);
#7813=VECTOR('',#29926,1000.);
#7814=VECTOR('',#29927,1000.);
#7815=VECTOR('',#29928,1000.);
#7816=VECTOR('',#29929,1000.);
#7817=VECTOR('',#29930,1000.);
#7818=VECTOR('',#29937,2.5);
#7819=VECTOR('',#29940,1000.);
#7820=VECTOR('',#29941,1000.);
#7821=VECTOR('',#29942,1000.);
#7822=VECTOR('',#29943,1000.);
#7823=VECTOR('',#29944,1000.);
#7824=VECTOR('',#29945,1000.);
#7825=VECTOR('',#29948,1000.);
#7826=VECTOR('',#29949,1000.);
#7827=VECTOR('',#29952,1000.);
#7828=VECTOR('',#29955,1000.);
#7829=VECTOR('',#29958,1000.);
#7830=VECTOR('',#29961,1000.);
#9608=CIRCLE('',#25809,2.5);
#9609=CIRCLE('',#25811,2.5);
#11074=VERTEX_POINT('',#52196);
#11075=VERTEX_POINT('',#52198);
#11076=VERTEX_POINT('',#52199);
#11077=VERTEX_POINT('',#52201);
#11078=VERTEX_POINT('',#52203);
#11079=VERTEX_POINT('',#52205);
#11080=VERTEX_POINT('',#52207);
#11081=VERTEX_POINT('',#52211);
#11082=VERTEX_POINT('',#52216);
#11083=VERTEX_POINT('',#52217);
#11084=VERTEX_POINT('',#52219);
#11085=VERTEX_POINT('',#52221);
#11086=VERTEX_POINT('',#52223);
#11087=VERTEX_POINT('',#52225);
#13758=EDGE_CURVE('',#11074,#11074,#9608,.T.);
#13759=EDGE_CURVE('',#11075,#11076,#5845,.T.);
#13760=EDGE_CURVE('',#11076,#11077,#5846,.T.);
#13761=EDGE_CURVE('',#11077,#11078,#5847,.T.);
#13762=EDGE_CURVE('',#11078,#11079,#5848,.T.);
#13763=EDGE_CURVE('',#11079,#11080,#5849,.T.);
#13764=EDGE_CURVE('',#11080,#11075,#5850,.T.);
#13765=EDGE_CURVE('',#11081,#11081,#9609,.T.);
#13766=EDGE_CURVE('',#11074,#11081,#5851,.T.);
#13767=EDGE_CURVE('',#11082,#11083,#5852,.T.);
#13768=EDGE_CURVE('',#11084,#11082,#5853,.T.);
#13769=EDGE_CURVE('',#11085,#11084,#5854,.T.);
#13770=EDGE_CURVE('',#11086,#11085,#5855,.T.);
#13771=EDGE_CURVE('',#11087,#11086,#5856,.T.);
#13772=EDGE_CURVE('',#11083,#11087,#5857,.T.);
#13773=EDGE_CURVE('',#11082,#11080,#5858,.T.);
#13774=EDGE_CURVE('',#11083,#11075,#5859,.T.);
#13775=EDGE_CURVE('',#11084,#11079,#5860,.T.);
#13776=EDGE_CURVE('',#11085,#11078,#5861,.T.);
#13777=EDGE_CURVE('',#11086,#11077,#5862,.T.);
#13778=EDGE_CURVE('',#11087,#11076,#5863,.T.);
#18426=ORIENTED_EDGE('',*,*,#13758,.T.);
#18427=ORIENTED_EDGE('',*,*,#13759,.T.);
#18428=ORIENTED_EDGE('',*,*,#13760,.T.);
#18429=ORIENTED_EDGE('',*,*,#13761,.T.);
#18430=ORIENTED_EDGE('',*,*,#13762,.T.);
#18431=ORIENTED_EDGE('',*,*,#13763,.T.);
#18432=ORIENTED_EDGE('',*,*,#13764,.T.);
#18433=ORIENTED_EDGE('',*,*,#13765,.T.);
#18434=ORIENTED_EDGE('',*,*,#13758,.F.);
#18435=ORIENTED_EDGE('',*,*,#13766,.T.);
#18436=ORIENTED_EDGE('',*,*,#13765,.F.);
#18437=ORIENTED_EDGE('',*,*,#13766,.F.);
#18438=ORIENTED_EDGE('',*,*,#13767,.F.);
#18439=ORIENTED_EDGE('',*,*,#13768,.F.);
#18440=ORIENTED_EDGE('',*,*,#13769,.F.);
#18441=ORIENTED_EDGE('',*,*,#13770,.F.);
#18442=ORIENTED_EDGE('',*,*,#13771,.F.);
#18443=ORIENTED_EDGE('',*,*,#13772,.F.);
#18444=ORIENTED_EDGE('',*,*,#13764,.F.);
#18445=ORIENTED_EDGE('',*,*,#13773,.F.);
#18446=ORIENTED_EDGE('',*,*,#13767,.T.);
#18447=ORIENTED_EDGE('',*,*,#13774,.T.);
#18448=ORIENTED_EDGE('',*,*,#13763,.F.);
#18449=ORIENTED_EDGE('',*,*,#13775,.F.);
#18450=ORIENTED_EDGE('',*,*,#13768,.T.);
#18451=ORIENTED_EDGE('',*,*,#13773,.T.);
#18452=ORIENTED_EDGE('',*,*,#13762,.F.);
#18453=ORIENTED_EDGE('',*,*,#13776,.F.);
#18454=ORIENTED_EDGE('',*,*,#13769,.T.);
#18455=ORIENTED_EDGE('',*,*,#13775,.T.);
#18456=ORIENTED_EDGE('',*,*,#13761,.F.);
#18457=ORIENTED_EDGE('',*,*,#13777,.F.);
#18458=ORIENTED_EDGE('',*,*,#13770,.T.);
#18459=ORIENTED_EDGE('',*,*,#13776,.T.);
#18460=ORIENTED_EDGE('',*,*,#13760,.F.);
#18461=ORIENTED_EDGE('',*,*,#13778,.F.);
#18462=ORIENTED_EDGE('',*,*,#13771,.T.);
#18463=ORIENTED_EDGE('',*,*,#13777,.T.);
#18464=ORIENTED_EDGE('',*,*,#13759,.F.);
#18465=ORIENTED_EDGE('',*,*,#13774,.F.);
#18466=ORIENTED_EDGE('',*,*,#13772,.T.);
#18467=ORIENTED_EDGE('',*,*,#13778,.T.);
#22866=CYLINDRICAL_SURFACE('',#25812,2.5);
#23695=ADVANCED_FACE('',(#2703,#1148),#1600,.T.);
#23696=ADVANCED_FACE('',(#2704),#1601,.T.);
#23697=ADVANCED_FACE('',(#2705),#22866,.T.);
#23698=ADVANCED_FACE('',(#2706),#1602,.F.);
#23699=ADVANCED_FACE('',(#2707),#1603,.F.);
#23700=ADVANCED_FACE('',(#2708),#1604,.F.);
#23701=ADVANCED_FACE('',(#2709),#1605,.F.);
#23702=ADVANCED_FACE('',(#2710),#1606,.F.);
#23703=ADVANCED_FACE('',(#2711),#1607,.F.);
#23704=ADVANCED_FACE('',(#2712),#1608,.F.);
#24542=CLOSED_SHELL('',(#23695,#23696,#23697,#23698,#23699,#23700,#23701,
#23702,#23703,#23704));
#25807=AXIS2_PLACEMENT_3D('',#52194,#29919,#29920);
#25808=AXIS2_PLACEMENT_3D('',#52195,#29921,#29922);
#25809=AXIS2_PLACEMENT_3D('',#52197,#29923,#29924);
#25810=AXIS2_PLACEMENT_3D('',#52210,#29931,#29932);
#25811=AXIS2_PLACEMENT_3D('',#52212,#29933,#29934);
#25812=AXIS2_PLACEMENT_3D('',#52213,#29935,#29936);
#25813=AXIS2_PLACEMENT_3D('',#52215,#29938,#29939);
#25814=AXIS2_PLACEMENT_3D('',#52228,#29946,#29947);
#25815=AXIS2_PLACEMENT_3D('',#52231,#29950,#29951);
#25816=AXIS2_PLACEMENT_3D('',#52233,#29953,#29954);
#25817=AXIS2_PLACEMENT_3D('',#52235,#29956,#29957);
#25818=AXIS2_PLACEMENT_3D('',#52237,#29959,#29960);
#25819=AXIS2_PLACEMENT_3D('',#52239,#29962,#29963);
#29919=DIRECTION('axis',(0.,0.,1.));
#29920=DIRECTION('refdir',(1.,0.,0.));
#29921=DIRECTION('center_axis',(0.,0.,-1.));
#29922=DIRECTION('ref_axis',(0.,-1.,0.));
#29923=DIRECTION('center_axis',(0.,0.,-1.));
#29924=DIRECTION('ref_axis',(1.,0.,0.));
#29925=DIRECTION('',(0.866025403761798,0.500000000039214,0.));
#29926=DIRECTION('',(0.,1.,0.));
#29927=DIRECTION('',(-0.866025403761798,0.500000000039214,0.));
#29928=DIRECTION('',(-0.866025403761798,-0.500000000039214,0.));
#29929=DIRECTION('',(0.,-1.,0.));
#29930=DIRECTION('',(0.866025403761798,-0.500000000039214,0.));
#29931=DIRECTION('center_axis',(0.,0.,1.));
#29932=DIRECTION('ref_axis',(1.,0.,0.));
#29933=DIRECTION('center_axis',(0.,0.,1.));
#29934=DIRECTION('ref_axis',(1.,0.,0.));
#29935=DIRECTION('center_axis',(0.,0.,-1.));
#29936=DIRECTION('ref_axis',(1.,0.,0.));
#29937=DIRECTION('',(0.,0.,1.));
#29938=DIRECTION('center_axis',(0.,0.,1.));
#29939=DIRECTION('ref_axis',(1.,0.,0.));
#29940=DIRECTION('',(0.866025403761798,-0.500000000039214,0.));
#29941=DIRECTION('',(0.,-1.,0.));
#29942=DIRECTION('',(-0.866025403761798,-0.500000000039214,0.));
#29943=DIRECTION('',(-0.866025403761798,0.500000000039214,0.));
#29944=DIRECTION('',(0.,1.,0.));
#29945=DIRECTION('',(0.866025403761798,0.500000000039214,0.));
#29946=DIRECTION('center_axis',(-0.500000000039214,-0.866025403761798,0.));
#29947=DIRECTION('ref_axis',(-0.866025403761798,0.500000000039214,0.));
#29948=DIRECTION('',(0.,0.,-1.));
#29949=DIRECTION('',(0.,0.,-1.));
#29950=DIRECTION('center_axis',(-1.,0.,0.));
#29951=DIRECTION('ref_axis',(0.,0.,1.));
#29952=DIRECTION('',(0.,0.,-1.));
#29953=DIRECTION('center_axis',(-0.500000000039214,0.866025403761798,0.));
#29954=DIRECTION('ref_axis',(0.,0.,1.));
#29955=DIRECTION('',(0.,0.,-1.));
#29956=DIRECTION('center_axis',(0.500000000039214,0.866025403761798,0.));
#29957=DIRECTION('ref_axis',(0.,0.,-1.));
#29958=DIRECTION('',(0.,0.,-1.));
#29959=DIRECTION('center_axis',(1.,0.,0.));
#29960=DIRECTION('ref_axis',(0.,1.,0.));
#29961=DIRECTION('',(0.,0.,-1.));
#29962=DIRECTION('center_axis',(0.500000000039214,-0.866025403761798,0.));
#29963=DIRECTION('ref_axis',(0.,0.,-1.));
#52194=CARTESIAN_POINT('',(0.,0.,0.));
#52195=CARTESIAN_POINT('Origin',(-23.,0.,-18.4));
#52196=CARTESIAN_POINT('',(-25.5,-3.06161699786838E-16,-18.4));
#52197=CARTESIAN_POINT('Origin',(-23.,0.,-18.4));
#52198=CARTESIAN_POINT('',(-23.,-1.3856406461,-18.4));
#52199=CARTESIAN_POINT('',(-21.8,-0.692820323,-18.4));
#52200=CARTESIAN_POINT('',(-22.3999999999746,-1.03923048453533,-18.4));
#52201=CARTESIAN_POINT('',(-21.8,0.692820323,-18.4));
#52202=CARTESIAN_POINT('',(-21.8,0.17320508075,-18.4));
#52203=CARTESIAN_POINT('',(-23.,1.3856406461,-18.4));
#52204=CARTESIAN_POINT('',(-22.3999999999746,1.03923048453533,-18.4));
#52205=CARTESIAN_POINT('',(-24.2,0.692820323,-18.4));
#52206=CARTESIAN_POINT('',(-23.6000000000254,1.03923048453533,-18.4));
#52207=CARTESIAN_POINT('',(-24.2,-0.692820323,-18.4));
#52208=CARTESIAN_POINT('',(-24.2,0.,-18.4));
#52209=CARTESIAN_POINT('',(-23.6000000000254,-1.03923048453533,-18.4));
#52210=CARTESIAN_POINT('Origin',(-23.,0.,-6.4));
#52211=CARTESIAN_POINT('',(-25.5,-3.06161699786838E-16,-6.4));
#52212=CARTESIAN_POINT('Origin',(-23.,0.,-6.4));
#52213=CARTESIAN_POINT('Origin',(-23.,0.,-12.4));
#52214=CARTESIAN_POINT('',(-25.5,3.06161699786838E-16,-12.4));
#52215=CARTESIAN_POINT('Origin',(-23.,3.11198878113149E-17,-15.9));
#52216=CARTESIAN_POINT('',(-24.2,-0.692820323,-15.9));
#52217=CARTESIAN_POINT('',(-23.,-1.3856406461,-15.9));
#52218=CARTESIAN_POINT('',(-24.2,-0.692820323,-15.9));
#52219=CARTESIAN_POINT('',(-24.2,0.692820323,-15.9));
#52220=CARTESIAN_POINT('',(-24.2,0.692820323,-15.9));
#52221=CARTESIAN_POINT('',(-23.,1.3856406461,-15.9));
#52222=CARTESIAN_POINT('',(-23.,1.3856406461,-15.9));
#52223=CARTESIAN_POINT('',(-21.8,0.692820323,-15.9));
#52224=CARTESIAN_POINT('',(-21.8,0.692820323,-15.9));
#52225=CARTESIAN_POINT('',(-21.8,-0.692820323,-15.9));
#52226=CARTESIAN_POINT('',(-21.8,-0.692820323,-15.9));
#52227=CARTESIAN_POINT('',(-23.,-1.3856406461,-15.9));
#52228=CARTESIAN_POINT('Origin',(-23.6,-1.03923048455,-15.9));
#52229=CARTESIAN_POINT('',(-24.2,-0.692820323,-15.9));
#52230=CARTESIAN_POINT('',(-23.,-1.3856406461,-15.9));
#52231=CARTESIAN_POINT('Origin',(-24.2,0.,-15.9));
#52232=CARTESIAN_POINT('',(-24.2,0.692820323,-15.9));
#52233=CARTESIAN_POINT('Origin',(-23.6,1.03923048455,-15.9));
#52234=CARTESIAN_POINT('',(-23.,1.3856406461,-15.9));
#52235=CARTESIAN_POINT('Origin',(-22.4,1.03923048455,-15.9));
#52236=CARTESIAN_POINT('',(-21.8,0.692820323,-15.9));
#52237=CARTESIAN_POINT('Origin',(-21.8,0.3464101615,-15.9));
#52238=CARTESIAN_POINT('',(-21.8,-0.692820323,-15.9));
#52239=CARTESIAN_POINT('Origin',(-22.4,-1.03923048455,-15.9));
#57023=UNCERTAINTY_MEASURE_WITH_UNIT(LENGTH_MEASURE(0.01),#57080,
'DISTANCE_ACCURACY_VALUE',
'Maximum model space distance between geometric entities at asserted c
onnectivities');
#57040=UNCERTAINTY_MEASURE_WITH_UNIT(LENGTH_MEASURE(0.01),#57080,
'DISTANCE_ACCURACY_VALUE',
'Maximum model space distance between geometric entities at asserted c
onnectivities');
#57062=(
GEOMETRIC_REPRESENTATION_CONTEXT(3)
GLOBAL_UNCERTAINTY_ASSIGNED_CONTEXT((#57023))
GLOBAL_UNIT_ASSIGNED_CONTEXT((#57080,#57082,#57083))
REPRESENTATION_CONTEXT('','3D')
);
#57079=(
GEOMETRIC_REPRESENTATION_CONTEXT(3)
GLOBAL_UNCERTAINTY_ASSIGNED_CONTEXT((#57040))
GLOBAL_UNIT_ASSIGNED_CONTEXT((#57080,#57082,#57083))
REPRESENTATION_CONTEXT('','3D')
);
#57080=(
LENGTH_UNIT()
NAMED_UNIT(*)
SI_UNIT(.MILLI.,.METRE.)
);
#57082=(
NAMED_UNIT(*)
PLANE_ANGLE_UNIT()
SI_UNIT($,.RADIAN.)
);
#57083=(
NAMED_UNIT(*)
SI_UNIT($,.STERADIAN.)
SOLID_ANGLE_UNIT()
);
#57105=SHAPE_DEFINITION_REPRESENTATION(#57151,#57270);
#57151=PRODUCT_DEFINITION_SHAPE('',$,#57309);
#57270=SHAPE_REPRESENTATION('',(#25807),#57062);
#57287=PRODUCT_DEFINITION_CONTEXT('part definition',#57403,'design');
#57309=PRODUCT_DEFINITION('Coupling Set Screw 2','Coupling Set Screw 2',
#57347,#57287);
#57347=PRODUCT_DEFINITION_FORMATION('',$,#57426);
#57403=APPLICATION_CONTEXT(
'Core Data for Automotive Mechanical Design Process');
#57404=PRODUCT_CONTEXT('part definition',#57403,'mechanical');
#57426=PRODUCT('Coupling Set Screw 2','Coupling Set Screw 2',$,(#57404));
#57444=PRESENTATION_STYLE_ASSIGNMENT((#57446));
#57446=SURFACE_STYLE_USAGE(.BOTH.,#57448);
#57448=SURFACE_SIDE_STYLE('',(#57450));
#57450=SURFACE_STYLE_FILL_AREA(#57452);
#57452=FILL_AREA_STYLE('Opaque(202,209,238)',(#57454));
#57454=FILL_AREA_STYLE_COLOUR('Opaque(202,209,238)',#57456);
#57456=COLOUR_RGB('Opaque(202,209,238)',0.792156862745098,0.819607843137255,
0.933333333333333);
ENDSEC;
END-ISO-10303-21;
